ISO-10303-21;
HEADER;
/* Generated by software containing ST-Developer
 * from STEP Tools, Inc. (www.steptools.com) 
 */

FILE_DESCRIPTION(
/* description */ ('Shaft runout checking stand'),
/* implementation_level */ '2;1');

FILE_NAME(
/* name */ 'Foot strip (1).step',
/* time_stamp */ '2026-11-02T21:12:33-08:00',
/* author */ (''),
/* organization */ (''),
/* preprocessor_version */ 'ST-DEVELOPER v20.2',
/* originating_system */ 'Autodesk Translation Framework v15.17.0.0',
/* authorisation */ '');

FILE_SCHEMA (('AUTOMOTIVE_DESIGN { 1 0 10303 214 3 1 1 }'));
ENDSEC;

DATA;
#10=MECHANICAL_DESIGN_GEOMETRIC_PRESENTATION_REPRESENTATION('',(#468),#11748);
#382=SHAPE_REPRESENTATION_RELATIONSHIP('SRR','None',#11931,#425);
#425=ADVANCED_BREP_SHAPE_REPRESENTATION('',(#519),#11707);
#468=STYLED_ITEM('',(#12171),#519);
#519=MANIFOLD_SOLID_BREP('Body1',#6211);
#1128=FACE_OUTER_BOUND('',#1525,.T.);
#1129=FACE_OUTER_BOUND('',#1526,.T.);
#1130=FACE_OUTER_BOUND('',#1527,.T.);
#1131=FACE_OUTER_BOUND('',#1528,.T.);
#1132=FACE_OUTER_BOUND('',#1529,.T.);
#1133=FACE_OUTER_BOUND('',#1530,.T.);
#1525=EDGE_LOOP('',(#4572,#4573,#4574,#4575));
#1526=EDGE_LOOP('',(#4576,#4577,#4578,#4579));
#1527=EDGE_LOOP('',(#4580,#4581,#4582,#4583));
#1528=EDGE_LOOP('',(#4584,#4585,#4586,#4587));
#1529=EDGE_LOOP('',(#4588,#4589,#4590,#4591));
#1530=EDGE_LOOP('',(#4592,#4593,#4594,#4595));
#2090=LINE('',#9979,#2557);
#2091=LINE('',#9981,#2558);
#2092=LINE('',#9983,#2559);
#2093=LINE('',#9984,#2560);
#2094=LINE('',#9987,#2561);
#2095=LINE('',#9989,#2562);
#2096=LINE('',#9990,#2563);
#2097=LINE('',#9993,#2564);
#2098=LINE('',#9995,#2565);
#2099=LINE('',#9996,#2566);
#2100=LINE('',#9998,#2567);
#2101=LINE('',#9999,#2568);
#2557=VECTOR('',#7969,1.);
#2558=VECTOR('',#7970,1.);
#2559=VECTOR('',#7971,1.);
#2560=VECTOR('',#7972,1.);
#2561=VECTOR('',#7975,1.);
#2562=VECTOR('',#7976,1.);
#2563=VECTOR('',#7977,1.);
#2564=VECTOR('',#7980,1.);
#2565=VECTOR('',#7981,1.);
#2566=VECTOR('',#7982,1.);
#2567=VECTOR('',#7985,1.);
#2568=VECTOR('',#7986,1.);
#2980=VERTEX_POINT('',#9977);
#2981=VERTEX_POINT('',#9978);
#2982=VERTEX_POINT('',#9980);
#2983=VERTEX_POINT('',#9982);
#2984=VERTEX_POINT('',#9986);
#2985=VERTEX_POINT('',#9988);
#2986=VERTEX_POINT('',#9992);
#2987=VERTEX_POINT('',#9994);
#3572=EDGE_CURVE('',#2980,#2981,#2090,.T.);
#3573=EDGE_CURVE('',#2981,#2982,#2091,.T.);
#3574=EDGE_CURVE('',#2983,#2982,#2092,.T.);
#3575=EDGE_CURVE('',#2980,#2983,#2093,.T.);
#3576=EDGE_CURVE('',#2984,#2980,#2094,.T.);
#3577=EDGE_CURVE('',#2985,#2983,#2095,.T.);
#3578=EDGE_CURVE('',#2984,#2985,#2096,.T.);
#3579=EDGE_CURVE('',#2986,#2984,#2097,.T.);
#3580=EDGE_CURVE('',#2987,#2985,#2098,.T.);
#3581=EDGE_CURVE('',#2986,#2987,#2099,.T.);
#3582=EDGE_CURVE('',#2981,#2986,#2100,.T.);
#3583=EDGE_CURVE('',#2982,#2987,#2101,.T.);
#4572=ORIENTED_EDGE('',*,*,#3572,.T.);
#4573=ORIENTED_EDGE('',*,*,#3573,.T.);
#4574=ORIENTED_EDGE('',*,*,#3574,.F.);
#4575=ORIENTED_EDGE('',*,*,#3575,.F.);
#4576=ORIENTED_EDGE('',*,*,#3576,.T.);
#4577=ORIENTED_EDGE('',*,*,#3575,.T.);
#4578=ORIENTED_EDGE('',*,*,#3577,.F.);
#4579=ORIENTED_EDGE('',*,*,#3578,.F.);
#4580=ORIENTED_EDGE('',*,*,#3579,.T.);
#4581=ORIENTED_EDGE('',*,*,#3578,.T.);
#4582=ORIENTED_EDGE('',*,*,#3580,.F.);
#4583=ORIENTED_EDGE('',*,*,#3581,.F.);
#4584=ORIENTED_EDGE('',*,*,#3582,.T.);
#4585=ORIENTED_EDGE('',*,*,#3581,.T.);
#4586=ORIENTED_EDGE('',*,*,#3583,.F.);
#4587=ORIENTED_EDGE('',*,*,#3573,.F.);
#4588=ORIENTED_EDGE('',*,*,#3583,.T.);
#4589=ORIENTED_EDGE('',*,*,#3580,.T.);
#4590=ORIENTED_EDGE('',*,*,#3577,.T.);
#4591=ORIENTED_EDGE('',*,*,#3574,.T.);
#4592=ORIENTED_EDGE('',*,*,#3582,.F.);
#4593=ORIENTED_EDGE('',*,*,#3572,.F.);
#4594=ORIENTED_EDGE('',*,*,#3576,.F.);
#4595=ORIENTED_EDGE('',*,*,#3579,.F.);
#5677=PLANE('',#6869);
#5678=PLANE('',#6870);
#5679=PLANE('',#6871);
#5680=PLANE('',#6872);
#5681=PLANE('',#6873);
#5682=PLANE('',#6874);
#5928=ADVANCED_FACE('',(#1128),#5677,.T.);
#5929=ADVANCED_FACE('',(#1129),#5678,.T.);
#5930=ADVANCED_FACE('',(#1130),#5679,.T.);
#5931=ADVANCED_FACE('',(#1131),#5680,.T.);
#5932=ADVANCED_FACE('',(#1132),#5681,.T.);
#5933=ADVANCED_FACE('',(#1133),#5682,.F.);
#6211=CLOSED_SHELL('',(#5928,#5929,#5930,#5931,#5932,#5933));
#6868=AXIS2_PLACEMENT_3D('',#9975,#7965,#7966);
#6869=AXIS2_PLACEMENT_3D('',#9976,#7967,#7968);
#6870=AXIS2_PLACEMENT_3D('',#9985,#7973,#7974);
#6871=AXIS2_PLACEMENT_3D('',#9991,#7978,#7979);
#6872=AXIS2_PLACEMENT_3D('',#9997,#7983,#7984);
#6873=AXIS2_PLACEMENT_3D('',#10000,#7987,#7988);
#6874=AXIS2_PLACEMENT_3D('',#10001,#7989,#7990);
#7965=DIRECTION('axis',(0.,0.,1.));
#7966=DIRECTION('refdir',(1.,0.,0.));
#7967=DIRECTION('center_axis',(0.,1.,0.));
#7968=DIRECTION('ref_axis',(-1.,0.,0.));
#7969=DIRECTION('',(-1.,0.,0.));
#7970=DIRECTION('',(0.,0.,1.));
#7971=DIRECTION('',(-1.,0.,0.));
#7972=DIRECTION('',(0.,0.,1.));
#7973=DIRECTION('center_axis',(1.,0.,0.));
#7974=DIRECTION('ref_axis',(0.,1.,0.));
#7975=DIRECTION('',(0.,1.,0.));
#7976=DIRECTION('',(0.,1.,0.));
#7977=DIRECTION('',(0.,0.,1.));
#7978=DIRECTION('center_axis',(0.,-1.,0.));
#7979=DIRECTION('ref_axis',(1.,0.,0.));
#7980=DIRECTION('',(1.,0.,0.));
#7981=DIRECTION('',(1.,0.,0.));
#7982=DIRECTION('',(0.,0.,1.));
#7983=DIRECTION('center_axis',(-1.,0.,0.));
#7984=DIRECTION('ref_axis',(0.,-1.,0.));
#7985=DIRECTION('',(0.,-1.,0.));
#7986=DIRECTION('',(0.,-1.,0.));
#7987=DIRECTION('center_axis',(0.,0.,1.));
#7988=DIRECTION('ref_axis',(1.,0.,0.));
#7989=DIRECTION('center_axis',(0.,0.,1.));
#7990=DIRECTION('ref_axis',(1.,0.,0.));
#9975=CARTESIAN_POINT('',(0.,0.,0.));
#9976=CARTESIAN_POINT('Origin',(5.,19.,-0.5));
#9977=CARTESIAN_POINT('',(5.,19.,-0.5));
#9978=CARTESIAN_POINT('',(-5.,19.,-0.5));
#9979=CARTESIAN_POINT('',(5.,19.,-0.5));
#9980=CARTESIAN_POINT('',(-5.,19.,0.));
#9981=CARTESIAN_POINT('',(-5.,19.,-0.5));
#9982=CARTESIAN_POINT('',(5.,19.,0.));
#9983=CARTESIAN_POINT('',(5.,19.,0.));
#9984=CARTESIAN_POINT('',(5.,19.,-0.5));
#9985=CARTESIAN_POINT('Origin',(5.,18.,-0.5));
#9986=CARTESIAN_POINT('',(5.,18.,-0.5));
#9987=CARTESIAN_POINT('',(5.,18.,-0.5));
#9988=CARTESIAN_POINT('',(5.,18.,0.));
#9989=CARTESIAN_POINT('',(5.,18.,0.));
#9990=CARTESIAN_POINT('',(5.,18.,-0.5));
#9991=CARTESIAN_POINT('Origin',(-5.,18.,-0.5));
#9992=CARTESIAN_POINT('',(-5.,18.,-0.5));
#9993=CARTESIAN_POINT('',(-5.,18.,-0.5));
#9994=CARTESIAN_POINT('',(-5.,18.,0.));
#9995=CARTESIAN_POINT('',(-5.,18.,0.));
#9996=CARTESIAN_POINT('',(-5.,18.,-0.5));
#9997=CARTESIAN_POINT('Origin',(-5.,19.,-0.5));
#9998=CARTESIAN_POINT('',(-5.,19.,-0.5));
#9999=CARTESIAN_POINT('',(-5.,19.,0.));
#10000=CARTESIAN_POINT('Origin',(0.,18.5,0.));
#10001=CARTESIAN_POINT('Origin',(0.,18.5,-0.5));
#11658=UNCERTAINTY_MEASURE_WITH_UNIT(LENGTH_MEASURE(0.001),#11749,
'DISTANCE_ACCURACY_VALUE',
'Maximum model space distance between geometric entities at asserted c
onnectivities');
#11699=UNCERTAINTY_MEASURE_WITH_UNIT(LENGTH_MEASURE(0.001),#11749,
'DISTANCE_ACCURACY_VALUE',
'Maximum model space distance between geometric entities at asserted c
onnectivities');
#11707=(
GEOMETRIC_REPRESENTATION_CONTEXT(3)
GLOBAL_UNCERTAINTY_ASSIGNED_CONTEXT((#11658))
GLOBAL_UNIT_ASSIGNED_CONTEXT((#11749,#11751,#11752))
REPRESENTATION_CONTEXT('','3D')
);
#11748=(
GEOMETRIC_REPRESENTATION_CONTEXT(3)
GLOBAL_UNCERTAINTY_ASSIGNED_CONTEXT((#11699))
GLOBAL_UNIT_ASSIGNED_CONTEXT((#11749,#11751,#11752))
REPRESENTATION_CONTEXT('','3D')
);
#11749=(
LENGTH_UNIT()
NAMED_UNIT(*)
SI_UNIT(.CENTI.,.METRE.)
);
#11751=(
NAMED_UNIT(*)
PLANE_ANGLE_UNIT()
SI_UNIT($,.RADIAN.)
);
#11752=(
NAMED_UNIT(*)
SI_UNIT($,.STERADIAN.)
SOLID_ANGLE_UNIT()
);
#11760=SHAPE_DEFINITION_REPRESENTATION(#11808,#11931);
#11808=PRODUCT_DEFINITION_SHAPE('',$,#11980);
#11931=SHAPE_REPRESENTATION('',(#6868),#11707);
#11972=PRODUCT_DEFINITION_CONTEXT('part definition',#12118,'design');
#11980=PRODUCT_DEFINITION('Foot strip_1','Foot strip (1)',#12028,#11972);
#12028=PRODUCT_DEFINITION_FORMATION('',$,#12127);
#12118=APPLICATION_CONTEXT(
'Core Data for Automotive Mechanical Design Process');
#12119=PRODUCT_CONTEXT('part definition',#12118,'mechanical');
#12127=PRODUCT('Foot strip_1','Foot strip (1)','Foot strip',(#12119));
#12171=PRESENTATION_STYLE_ASSIGNMENT((#12176));
#12176=SURFACE_STYLE_USAGE(.BOTH.,#12181);
#12181=SURFACE_SIDE_STYLE('',(#12186));
#12186=SURFACE_STYLE_FILL_AREA(#12191);
#12191=FILL_AREA_STYLE('CAD Library Painted - Deep blue',(#12196));
#12196=FILL_AREA_STYLE_COLOUR('CAD Library Painted - Deep blue',#12201);
#12201=COLOUR_RGB('CAD Library Painted - Deep blue',0.0784313725490196,
0.203921568627451,0.349019607843137);
ENDSEC;
END-ISO-10303-21;
